ISO-10303-21;
HEADER;
/* Generated by software containing ST-Developer
 * from STEP Tools, Inc. (www.steptools.com) 
 */

FILE_DESCRIPTION(
/* description */ ('Lifting hook block with sheave'),
/* implementation_level */ '2;1');

FILE_NAME(
/* name */ 'Side plate (1).step',
/* time_stamp */ '2026-10-28T03:23:54-07:00',
/* author */ (''),
/* organization */ (''),
/* preprocessor_version */ 'ST-DEVELOPER v20.2',
/* originating_system */ 'Autodesk Translation Framework v15.17.0.0',
/* authorisation */ '');

FILE_SCHEMA (('AUTOMOTIVE_DESIGN { 1 0 10303 214 3 1 1 }'));
ENDSEC;

DATA;
#10=MECHANICAL_DESIGN_GEOMETRIC_PRESENTATION_REPRESENTATION('',(#352),#9391);
#292=SHAPE_REPRESENTATION_RELATIONSHIP('SRR','None',#9523,#322);
#322=ADVANCED_BREP_SHAPE_REPRESENTATION('',(#390),#9358);
#352=STYLED_ITEM('',(#9752),#390);
#390=MANIFOLD_SOLID_BREP('Body1',#4888);
#465=LINE('',#7732,#753);
#466=LINE('',#7734,#754);
#467=LINE('',#7738,#755);
#468=LINE('',#7740,#756);
#469=LINE('',#7744,#757);
#470=LINE('',#7747,#758);
#471=LINE('',#7751,#759);
#472=LINE('',#7754,#760);
#473=LINE('',#7757,#761);
#474=LINE('',#7762,#762);
#475=LINE('',#7769,#763);
#476=LINE('',#7779,#764);
#477=LINE('',#7786,#765);
#478=LINE('',#7793,#766);
#479=LINE('',#7799,#767);
#480=LINE('',#7805,#768);
#481=LINE('',#7809,#769);
#482=LINE('',#7814,#770);
#483=LINE('',#7816,#771);
#484=LINE('',#7818,#772);
#485=LINE('',#7819,#773);
#486=LINE('',#7822,#774);
#487=LINE('',#7824,#775);
#488=LINE('',#7825,#776);
#489=LINE('',#7828,#777);
#490=LINE('',#7830,#778);
#491=LINE('',#7831,#779);
#492=LINE('',#7834,#780);
#493=LINE('',#7836,#781);
#494=LINE('',#7837,#782);
#495=LINE('',#7840,#783);
#496=LINE('',#7842,#784);
#497=LINE('',#7843,#785);
#498=LINE('',#7846,#786);
#499=LINE('',#7848,#787);
#500=LINE('',#7849,#788);
#501=LINE('',#7852,#789);
#502=LINE('',#7854,#790);
#503=LINE('',#7855,#791);
#504=LINE('',#7857,#792);
#505=LINE('',#7858,#793);
#753=VECTOR('',#6118,1.);
#754=VECTOR('',#6119,1.);
#755=VECTOR('',#6124,1.);
#756=VECTOR('',#6125,1.);
#757=VECTOR('',#6130,1.);
#758=VECTOR('',#6133,1.);
#759=VECTOR('',#6138,1.2);
#760=VECTOR('',#6141,1.);
#761=VECTOR('',#6144,1.);
#762=VECTOR('',#6149,0.9);
#763=VECTOR('',#6158,0.9);
#764=VECTOR('',#6171,0.9);
#765=VECTOR('',#6180,0.9);
#766=VECTOR('',#6189,0.425);
#767=VECTOR('',#6196,0.425);
#768=VECTOR('',#6203,0.425);
#769=VECTOR('',#6208,1.);
#770=VECTOR('',#6213,1.);
#771=VECTOR('',#6214,1.);
#772=VECTOR('',#6215,1.);
#773=VECTOR('',#6216,1.);
#774=VECTOR('',#6219,1.);
#775=VECTOR('',#6220,1.);
#776=VECTOR('',#6221,1.);
#777=VECTOR('',#6224,1.);
#778=VECTOR('',#6225,1.);
#779=VECTOR('',#6226,1.);
#780=VECTOR('',#6229,1.);
#781=VECTOR('',#6230,1.);
#782=VECTOR('',#6231,1.);
#783=VECTOR('',#6234,1.);
#784=VECTOR('',#6235,1.);
#785=VECTOR('',#6236,1.);
#786=VECTOR('',#6239,1.);
#787=VECTOR('',#6240,1.);
#788=VECTOR('',#6241,1.);
#789=VECTOR('',#6244,1.);
#790=VECTOR('',#6245,1.);
#791=VECTOR('',#6246,1.);
#792=VECTOR('',#6249,1.);
#793=VECTOR('',#6250,1.);
#1013=CYLINDRICAL_SURFACE('',#5332,3.25);
#1014=CYLINDRICAL_SURFACE('',#5334,3.25);
#1015=CYLINDRICAL_SURFACE('',#5336,3.25);
#1016=CYLINDRICAL_SURFACE('',#5338,1.2);
#1017=CYLINDRICAL_SURFACE('',#5340,3.25);
#1018=CYLINDRICAL_SURFACE('',#5342,0.9);
#1019=CYLINDRICAL_SURFACE('',#5346,0.9);
#1020=CYLINDRICAL_SURFACE('',#5352,0.9);
#1021=CYLINDRICAL_SURFACE('',#5356,0.9);
#1022=CYLINDRICAL_SURFACE('',#5360,0.425);
#1023=CYLINDRICAL_SURFACE('',#5363,0.425);
#1024=CYLINDRICAL_SURFACE('',#5366,0.425);
#1025=CYLINDRICAL_SURFACE('',#5369,1.);
#1121=FACE_BOUND('',#1551,.T.);
#1122=FACE_BOUND('',#1560,.T.);
#1123=FACE_BOUND('',#1576,.T.);
#1124=FACE_BOUND('',#1577,.T.);
#1125=FACE_BOUND('',#1578,.T.);
#1126=FACE_BOUND('',#1579,.T.);
#1127=FACE_BOUND('',#1580,.T.);
#1128=FACE_BOUND('',#1581,.T.);
#1129=FACE_BOUND('',#1582,.T.);
#1130=FACE_BOUND('',#1583,.T.);
#1131=FACE_BOUND('',#1585,.T.);
#1132=FACE_BOUND('',#1586,.T.);
#1133=FACE_BOUND('',#1587,.T.);
#1134=FACE_BOUND('',#1588,.T.);
#1247=FACE_OUTER_BOUND('',#1550,.T.);
#1248=FACE_OUTER_BOUND('',#1552,.T.);
#1249=FACE_OUTER_BOUND('',#1553,.T.);
#1250=FACE_OUTER_BOUND('',#1554,.T.);
#1251=FACE_OUTER_BOUND('',#1555,.T.);
#1252=FACE_OUTER_BOUND('',#1556,.T.);
#1253=FACE_OUTER_BOUND('',#1557,.T.);
#1254=FACE_OUTER_BOUND('',#1558,.T.);
#1255=FACE_OUTER_BOUND('',#1559,.T.);
#1256=FACE_OUTER_BOUND('',#1561,.T.);
#1257=FACE_OUTER_BOUND('',#1562,.T.);
#1258=FACE_OUTER_BOUND('',#1563,.T.);
#1259=FACE_OUTER_BOUND('',#1564,.T.);
#1260=FACE_OUTER_BOUND('',#1565,.T.);
#1261=FACE_OUTER_BOUND('',#1566,.T.);
#1262=FACE_OUTER_BOUND('',#1567,.T.);
#1263=FACE_OUTER_BOUND('',#1568,.T.);
#1264=FACE_OUTER_BOUND('',#1569,.T.);
#1265=FACE_OUTER_BOUND('',#1570,.T.);
#1266=FACE_OUTER_BOUND('',#1571,.T.);
#1267=FACE_OUTER_BOUND('',#1572,.T.);
#1268=FACE_OUTER_BOUND('',#1573,.T.);
#1269=FACE_OUTER_BOUND('',#1574,.T.);
#1270=FACE_OUTER_BOUND('',#1575,.T.);
#1271=FACE_OUTER_BOUND('',#1584,.T.);
#1550=EDGE_LOOP('',(#3380,#3381,#3382,#3383,#3384,#3385,#3386,#3387));
#1551=EDGE_LOOP('',(#3388));
#1552=EDGE_LOOP('',(#3389,#3390,#3391,#3392));
#1553=EDGE_LOOP('',(#3393,#3394,#3395,#3396));
#1554=EDGE_LOOP('',(#3397,#3398,#3399,#3400));
#1555=EDGE_LOOP('',(#3401,#3402,#3403,#3404));
#1556=EDGE_LOOP('',(#3405,#3406,#3407,#3408));
#1557=EDGE_LOOP('',(#3409,#3410,#3411,#3412,#3413,#3414,#3415,#3416));
#1558=EDGE_LOOP('',(#3417,#3418,#3419,#3420,#3421,#3422,#3423,#3424));
#1559=EDGE_LOOP('',(#3425));
#1560=EDGE_LOOP('',(#3426));
#1561=EDGE_LOOP('',(#3427,#3428,#3429,#3430,#3431,#3432,#3433,#3434));
#1562=EDGE_LOOP('',(#3435,#3436,#3437,#3438,#3439,#3440,#3441,#3442));
#1563=EDGE_LOOP('',(#3443,#3444,#3445,#3446));
#1564=EDGE_LOOP('',(#3447,#3448,#3449,#3450));
#1565=EDGE_LOOP('',(#3451,#3452,#3453,#3454));
#1566=EDGE_LOOP('',(#3455,#3456,#3457,#3458));
#1567=EDGE_LOOP('',(#3459,#3460,#3461,#3462));
#1568=EDGE_LOOP('',(#3463,#3464,#3465,#3466));
#1569=EDGE_LOOP('',(#3467,#3468,#3469,#3470));
#1570=EDGE_LOOP('',(#3471,#3472,#3473,#3474));
#1571=EDGE_LOOP('',(#3475,#3476,#3477,#3478));
#1572=EDGE_LOOP('',(#3479,#3480,#3481,#3482));
#1573=EDGE_LOOP('',(#3483,#3484,#3485,#3486));
#1574=EDGE_LOOP('',(#3487,#3488,#3489,#3490));
#1575=EDGE_LOOP('',(#3491,#3492,#3493,#3494,#3495,#3496,#3497,#3498));
#1576=EDGE_LOOP('',(#3499));
#1577=EDGE_LOOP('',(#3500));
#1578=EDGE_LOOP('',(#3501));
#1579=EDGE_LOOP('',(#3502));
#1580=EDGE_LOOP('',(#3503));
#1581=EDGE_LOOP('',(#3504));
#1582=EDGE_LOOP('',(#3505));
#1583=EDGE_LOOP('',(#3506));
#1584=EDGE_LOOP('',(#3507,#3508,#3509,#3510,#3511,#3512,#3513,#3514));
#1585=EDGE_LOOP('',(#3515,#3516,#3517,#3518,#3519,#3520,#3521,#3522,#3523,
#3524,#3525,#3526));
#1586=EDGE_LOOP('',(#3527));
#1587=EDGE_LOOP('',(#3528));
#1588=EDGE_LOOP('',(#3529));
#1949=CIRCLE('',#5323,0.9);
#1950=CIRCLE('',#5324,3.25);
#1951=CIRCLE('',#5325,0.9);
#1952=CIRCLE('',#5326,3.25);
#1953=CIRCLE('',#5327,0.9);
#1954=CIRCLE('',#5328,3.25);
#1955=CIRCLE('',#5329,0.9);
#1956=CIRCLE('',#5330,3.25);
#1957=CIRCLE('',#5331,1.2);
#1958=CIRCLE('',#5333,3.25);
#1959=CIRCLE('',#5335,3.25);
#1960=CIRCLE('',#5337,3.25);
#1961=CIRCLE('',#5339,1.2);
#1962=CIRCLE('',#5341,3.25);
#1963=CIRCLE('',#5343,0.9);
#1964=CIRCLE('',#5344,0.9);
#1965=CIRCLE('',#5345,0.9);
#1966=CIRCLE('',#5347,0.9);
#1967=CIRCLE('',#5348,0.9);
#1968=CIRCLE('',#5349,0.9);
#1969=CIRCLE('',#5351,1.);
#1970=CIRCLE('',#5353,0.9);
#1971=CIRCLE('',#5354,0.9);
#1972=CIRCLE('',#5355,0.9);
#1973=CIRCLE('',#5357,0.9);
#1974=CIRCLE('',#5358,0.9);
#1975=CIRCLE('',#5359,0.9);
#1976=CIRCLE('',#5361,0.425);
#1977=CIRCLE('',#5362,0.425);
#1978=CIRCLE('',#5364,0.425);
#1979=CIRCLE('',#5365,0.425);
#1980=CIRCLE('',#5367,0.425);
#1981=CIRCLE('',#5368,0.425);
#1982=CIRCLE('',#5370,1.);
#2258=VERTEX_POINT('',#7712);
#2259=VERTEX_POINT('',#7713);
#2260=VERTEX_POINT('',#7715);
#2261=VERTEX_POINT('',#7717);
#2262=VERTEX_POINT('',#7719);
#2263=VERTEX_POINT('',#7721);
#2264=VERTEX_POINT('',#7723);
#2265=VERTEX_POINT('',#7725);
#2266=VERTEX_POINT('',#7728);
#2267=VERTEX_POINT('',#7731);
#2268=VERTEX_POINT('',#7733);
#2269=VERTEX_POINT('',#7737);
#2270=VERTEX_POINT('',#7739);
#2271=VERTEX_POINT('',#7743);
#2272=VERTEX_POINT('',#7745);
#2273=VERTEX_POINT('',#7749);
#2274=VERTEX_POINT('',#7753);
#2275=VERTEX_POINT('',#7755);
#2276=VERTEX_POINT('',#7759);
#2277=VERTEX_POINT('',#7761);
#2278=VERTEX_POINT('',#7766);
#2279=VERTEX_POINT('',#7768);
#2280=VERTEX_POINT('',#7773);
#2281=VERTEX_POINT('',#7776);
#2282=VERTEX_POINT('',#7778);
#2283=VERTEX_POINT('',#7783);
#2284=VERTEX_POINT('',#7785);
#2285=VERTEX_POINT('',#7790);
#2286=VERTEX_POINT('',#7792);
#2287=VERTEX_POINT('',#7796);
#2288=VERTEX_POINT('',#7798);
#2289=VERTEX_POINT('',#7802);
#2290=VERTEX_POINT('',#7804);
#2291=VERTEX_POINT('',#7808);
#2292=VERTEX_POINT('',#7812);
#2293=VERTEX_POINT('',#7813);
#2294=VERTEX_POINT('',#7815);
#2295=VERTEX_POINT('',#7817);
#2296=VERTEX_POINT('',#7821);
#2297=VERTEX_POINT('',#7823);
#2298=VERTEX_POINT('',#7827);
#2299=VERTEX_POINT('',#7829);
#2300=VERTEX_POINT('',#7833);
#2301=VERTEX_POINT('',#7835);
#2302=VERTEX_POINT('',#7839);
#2303=VERTEX_POINT('',#7841);
#2304=VERTEX_POINT('',#7845);
#2305=VERTEX_POINT('',#7847);
#2306=VERTEX_POINT('',#7851);
#2307=VERTEX_POINT('',#7853);
#2694=EDGE_CURVE('',#2258,#2259,#1949,.T.);
#2695=EDGE_CURVE('',#2260,#2258,#1950,.T.);
#2696=EDGE_CURVE('',#2261,#2260,#1951,.T.);
#2697=EDGE_CURVE('',#2262,#2261,#1952,.T.);
#2698=EDGE_CURVE('',#2263,#2262,#1953,.T.);
#2699=EDGE_CURVE('',#2264,#2263,#1954,.T.);
#2700=EDGE_CURVE('',#2265,#2264,#1955,.T.);
#2701=EDGE_CURVE('',#2259,#2265,#1956,.T.);
#2702=EDGE_CURVE('',#2266,#2266,#1957,.T.);
#2703=EDGE_CURVE('',#2264,#2267,#465,.T.);
#2704=EDGE_CURVE('',#2268,#2263,#466,.T.);
#2705=EDGE_CURVE('',#2267,#2268,#1958,.T.);
#2706=EDGE_CURVE('',#2259,#2269,#467,.T.);
#2707=EDGE_CURVE('',#2270,#2265,#468,.T.);
#2708=EDGE_CURVE('',#2269,#2270,#1959,.T.);
#2709=EDGE_CURVE('',#2271,#2261,#469,.T.);
#2710=EDGE_CURVE('',#2272,#2271,#1960,.T.);
#2711=EDGE_CURVE('',#2262,#2272,#470,.T.);
#2712=EDGE_CURVE('',#2273,#2273,#1961,.T.);
#2713=EDGE_CURVE('',#2273,#2266,#471,.T.);
#2714=EDGE_CURVE('',#2274,#2258,#472,.T.);
#2715=EDGE_CURVE('',#2275,#2274,#1962,.T.);
#2716=EDGE_CURVE('',#2260,#2275,#473,.T.);
#2717=EDGE_CURVE('',#2276,#2269,#1963,.T.);
#2718=EDGE_CURVE('',#2276,#2277,#474,.T.);
#2719=EDGE_CURVE('',#2277,#2277,#1964,.T.);
#2720=EDGE_CURVE('',#2274,#2276,#1965,.T.);
#2721=EDGE_CURVE('',#2278,#2267,#1966,.T.);
#2722=EDGE_CURVE('',#2278,#2279,#475,.T.);
#2723=EDGE_CURVE('',#2279,#2279,#1967,.T.);
#2724=EDGE_CURVE('',#2270,#2278,#1968,.T.);
#2725=EDGE_CURVE('',#2280,#2280,#1969,.T.);
#2726=EDGE_CURVE('',#2281,#2275,#1970,.T.);
#2727=EDGE_CURVE('',#2281,#2282,#476,.T.);
#2728=EDGE_CURVE('',#2282,#2282,#1971,.T.);
#2729=EDGE_CURVE('',#2271,#2281,#1972,.T.);
#2730=EDGE_CURVE('',#2283,#2272,#1973,.T.);
#2731=EDGE_CURVE('',#2283,#2284,#477,.T.);
#2732=EDGE_CURVE('',#2284,#2284,#1974,.T.);
#2733=EDGE_CURVE('',#2268,#2283,#1975,.T.);
#2734=EDGE_CURVE('',#2285,#2285,#1976,.T.);
#2735=EDGE_CURVE('',#2285,#2286,#478,.T.);
#2736=EDGE_CURVE('',#2286,#2286,#1977,.T.);
#2737=EDGE_CURVE('',#2287,#2287,#1978,.T.);
#2738=EDGE_CURVE('',#2287,#2288,#479,.T.);
#2739=EDGE_CURVE('',#2288,#2288,#1979,.T.);
#2740=EDGE_CURVE('',#2289,#2289,#1980,.T.);
#2741=EDGE_CURVE('',#2289,#2290,#480,.T.);
#2742=EDGE_CURVE('',#2290,#2290,#1981,.T.);
#2743=EDGE_CURVE('',#2280,#2291,#481,.T.);
#2744=EDGE_CURVE('',#2291,#2291,#1982,.T.);
#2745=EDGE_CURVE('',#2292,#2293,#482,.T.);
#2746=EDGE_CURVE('',#2292,#2294,#483,.T.);
#2747=EDGE_CURVE('',#2295,#2294,#484,.T.);
#2748=EDGE_CURVE('',#2293,#2295,#485,.T.);
#2749=EDGE_CURVE('',#2293,#2296,#486,.T.);
#2750=EDGE_CURVE('',#2297,#2295,#487,.T.);
#2751=EDGE_CURVE('',#2296,#2297,#488,.T.);
#2752=EDGE_CURVE('',#2296,#2298,#489,.T.);
#2753=EDGE_CURVE('',#2299,#2297,#490,.T.);
#2754=EDGE_CURVE('',#2298,#2299,#491,.T.);
#2755=EDGE_CURVE('',#2298,#2300,#492,.T.);
#2756=EDGE_CURVE('',#2301,#2299,#493,.T.);
#2757=EDGE_CURVE('',#2300,#2301,#494,.T.);
#2758=EDGE_CURVE('',#2300,#2302,#495,.T.);
#2759=EDGE_CURVE('',#2303,#2301,#496,.T.);
#2760=EDGE_CURVE('',#2302,#2303,#497,.T.);
#2761=EDGE_CURVE('',#2302,#2304,#498,.T.);
#2762=EDGE_CURVE('',#2305,#2303,#499,.T.);
#2763=EDGE_CURVE('',#2304,#2305,#500,.T.);
#2764=EDGE_CURVE('',#2304,#2306,#501,.T.);
#2765=EDGE_CURVE('',#2307,#2305,#502,.T.);
#2766=EDGE_CURVE('',#2306,#2307,#503,.T.);
#2767=EDGE_CURVE('',#2306,#2292,#504,.T.);
#2768=EDGE_CURVE('',#2294,#2307,#505,.T.);
#3380=ORIENTED_EDGE('',*,*,#2694,.F.);
#3381=ORIENTED_EDGE('',*,*,#2695,.F.);
#3382=ORIENTED_EDGE('',*,*,#2696,.F.);
#3383=ORIENTED_EDGE('',*,*,#2697,.F.);
#3384=ORIENTED_EDGE('',*,*,#2698,.F.);
#3385=ORIENTED_EDGE('',*,*,#2699,.F.);
#3386=ORIENTED_EDGE('',*,*,#2700,.F.);
#3387=ORIENTED_EDGE('',*,*,#2701,.F.);
#3388=ORIENTED_EDGE('',*,*,#2702,.F.);
#3389=ORIENTED_EDGE('',*,*,#2703,.F.);
#3390=ORIENTED_EDGE('',*,*,#2699,.T.);
#3391=ORIENTED_EDGE('',*,*,#2704,.F.);
#3392=ORIENTED_EDGE('',*,*,#2705,.F.);
#3393=ORIENTED_EDGE('',*,*,#2706,.F.);
#3394=ORIENTED_EDGE('',*,*,#2701,.T.);
#3395=ORIENTED_EDGE('',*,*,#2707,.F.);
#3396=ORIENTED_EDGE('',*,*,#2708,.F.);
#3397=ORIENTED_EDGE('',*,*,#2709,.F.);
#3398=ORIENTED_EDGE('',*,*,#2710,.F.);
#3399=ORIENTED_EDGE('',*,*,#2711,.F.);
#3400=ORIENTED_EDGE('',*,*,#2697,.T.);
#3401=ORIENTED_EDGE('',*,*,#2712,.F.);
#3402=ORIENTED_EDGE('',*,*,#2713,.T.);
#3403=ORIENTED_EDGE('',*,*,#2702,.T.);
#3404=ORIENTED_EDGE('',*,*,#2713,.F.);
#3405=ORIENTED_EDGE('',*,*,#2714,.F.);
#3406=ORIENTED_EDGE('',*,*,#2715,.F.);
#3407=ORIENTED_EDGE('',*,*,#2716,.F.);
#3408=ORIENTED_EDGE('',*,*,#2695,.T.);
#3409=ORIENTED_EDGE('',*,*,#2714,.T.);
#3410=ORIENTED_EDGE('',*,*,#2694,.T.);
#3411=ORIENTED_EDGE('',*,*,#2706,.T.);
#3412=ORIENTED_EDGE('',*,*,#2717,.F.);
#3413=ORIENTED_EDGE('',*,*,#2718,.T.);
#3414=ORIENTED_EDGE('',*,*,#2719,.F.);
#3415=ORIENTED_EDGE('',*,*,#2718,.F.);
#3416=ORIENTED_EDGE('',*,*,#2720,.F.);
#3417=ORIENTED_EDGE('',*,*,#2707,.T.);
#3418=ORIENTED_EDGE('',*,*,#2700,.T.);
#3419=ORIENTED_EDGE('',*,*,#2703,.T.);
#3420=ORIENTED_EDGE('',*,*,#2721,.F.);
#3421=ORIENTED_EDGE('',*,*,#2722,.T.);
#3422=ORIENTED_EDGE('',*,*,#2723,.F.);
#3423=ORIENTED_EDGE('',*,*,#2722,.F.);
#3424=ORIENTED_EDGE('',*,*,#2724,.F.);
#3425=ORIENTED_EDGE('',*,*,#2712,.T.);
#3426=ORIENTED_EDGE('',*,*,#2725,.T.);
#3427=ORIENTED_EDGE('',*,*,#2716,.T.);
#3428=ORIENTED_EDGE('',*,*,#2726,.F.);
#3429=ORIENTED_EDGE('',*,*,#2727,.T.);
#3430=ORIENTED_EDGE('',*,*,#2728,.F.);
#3431=ORIENTED_EDGE('',*,*,#2727,.F.);
#3432=ORIENTED_EDGE('',*,*,#2729,.F.);
#3433=ORIENTED_EDGE('',*,*,#2709,.T.);
#3434=ORIENTED_EDGE('',*,*,#2696,.T.);
#3435=ORIENTED_EDGE('',*,*,#2711,.T.);
#3436=ORIENTED_EDGE('',*,*,#2730,.F.);
#3437=ORIENTED_EDGE('',*,*,#2731,.T.);
#3438=ORIENTED_EDGE('',*,*,#2732,.F.);
#3439=ORIENTED_EDGE('',*,*,#2731,.F.);
#3440=ORIENTED_EDGE('',*,*,#2733,.F.);
#3441=ORIENTED_EDGE('',*,*,#2704,.T.);
#3442=ORIENTED_EDGE('',*,*,#2698,.T.);
#3443=ORIENTED_EDGE('',*,*,#2734,.F.);
#3444=ORIENTED_EDGE('',*,*,#2735,.T.);
#3445=ORIENTED_EDGE('',*,*,#2736,.F.);
#3446=ORIENTED_EDGE('',*,*,#2735,.F.);
#3447=ORIENTED_EDGE('',*,*,#2737,.F.);
#3448=ORIENTED_EDGE('',*,*,#2738,.T.);
#3449=ORIENTED_EDGE('',*,*,#2739,.F.);
#3450=ORIENTED_EDGE('',*,*,#2738,.F.);
#3451=ORIENTED_EDGE('',*,*,#2740,.F.);
#3452=ORIENTED_EDGE('',*,*,#2741,.T.);
#3453=ORIENTED_EDGE('',*,*,#2742,.F.);
#3454=ORIENTED_EDGE('',*,*,#2741,.F.);
#3455=ORIENTED_EDGE('',*,*,#2725,.F.);
#3456=ORIENTED_EDGE('',*,*,#2743,.T.);
#3457=ORIENTED_EDGE('',*,*,#2744,.F.);
#3458=ORIENTED_EDGE('',*,*,#2743,.F.);
#3459=ORIENTED_EDGE('',*,*,#2745,.F.);
#3460=ORIENTED_EDGE('',*,*,#2746,.T.);
#3461=ORIENTED_EDGE('',*,*,#2747,.F.);
#3462=ORIENTED_EDGE('',*,*,#2748,.F.);
#3463=ORIENTED_EDGE('',*,*,#2749,.F.);
#3464=ORIENTED_EDGE('',*,*,#2748,.T.);
#3465=ORIENTED_EDGE('',*,*,#2750,.F.);
#3466=ORIENTED_EDGE('',*,*,#2751,.F.);
#3467=ORIENTED_EDGE('',*,*,#2752,.F.);
#3468=ORIENTED_EDGE('',*,*,#2751,.T.);
#3469=ORIENTED_EDGE('',*,*,#2753,.F.);
#3470=ORIENTED_EDGE('',*,*,#2754,.F.);
#3471=ORIENTED_EDGE('',*,*,#2755,.F.);
#3472=ORIENTED_EDGE('',*,*,#2754,.T.);
#3473=ORIENTED_EDGE('',*,*,#2756,.F.);
#3474=ORIENTED_EDGE('',*,*,#2757,.F.);
#3475=ORIENTED_EDGE('',*,*,#2758,.F.);
#3476=ORIENTED_EDGE('',*,*,#2757,.T.);
#3477=ORIENTED_EDGE('',*,*,#2759,.F.);
#3478=ORIENTED_EDGE('',*,*,#2760,.F.);
#3479=ORIENTED_EDGE('',*,*,#2761,.F.);
#3480=ORIENTED_EDGE('',*,*,#2760,.T.);
#3481=ORIENTED_EDGE('',*,*,#2762,.F.);
#3482=ORIENTED_EDGE('',*,*,#2763,.F.);
#3483=ORIENTED_EDGE('',*,*,#2764,.F.);
#3484=ORIENTED_EDGE('',*,*,#2763,.T.);
#3485=ORIENTED_EDGE('',*,*,#2765,.F.);
#3486=ORIENTED_EDGE('',*,*,#2766,.F.);
#3487=ORIENTED_EDGE('',*,*,#2767,.F.);
#3488=ORIENTED_EDGE('',*,*,#2766,.T.);
#3489=ORIENTED_EDGE('',*,*,#2768,.F.);
#3490=ORIENTED_EDGE('',*,*,#2746,.F.);
#3491=ORIENTED_EDGE('',*,*,#2768,.T.);
#3492=ORIENTED_EDGE('',*,*,#2765,.T.);
#3493=ORIENTED_EDGE('',*,*,#2762,.T.);
#3494=ORIENTED_EDGE('',*,*,#2759,.T.);
#3495=ORIENTED_EDGE('',*,*,#2756,.T.);
#3496=ORIENTED_EDGE('',*,*,#2753,.T.);
#3497=ORIENTED_EDGE('',*,*,#2750,.T.);
#3498=ORIENTED_EDGE('',*,*,#2747,.T.);
#3499=ORIENTED_EDGE('',*,*,#2744,.T.);
#3500=ORIENTED_EDGE('',*,*,#2742,.T.);
#3501=ORIENTED_EDGE('',*,*,#2739,.T.);
#3502=ORIENTED_EDGE('',*,*,#2736,.T.);
#3503=ORIENTED_EDGE('',*,*,#2732,.T.);
#3504=ORIENTED_EDGE('',*,*,#2719,.T.);
#3505=ORIENTED_EDGE('',*,*,#2723,.T.);
#3506=ORIENTED_EDGE('',*,*,#2728,.T.);
#3507=ORIENTED_EDGE('',*,*,#2767,.T.);
#3508=ORIENTED_EDGE('',*,*,#2745,.T.);
#3509=ORIENTED_EDGE('',*,*,#2749,.T.);
#3510=ORIENTED_EDGE('',*,*,#2752,.T.);
#3511=ORIENTED_EDGE('',*,*,#2755,.T.);
#3512=ORIENTED_EDGE('',*,*,#2758,.T.);
#3513=ORIENTED_EDGE('',*,*,#2761,.T.);
#3514=ORIENTED_EDGE('',*,*,#2764,.T.);
#3515=ORIENTED_EDGE('',*,*,#2715,.T.);
#3516=ORIENTED_EDGE('',*,*,#2720,.T.);
#3517=ORIENTED_EDGE('',*,*,#2717,.T.);
#3518=ORIENTED_EDGE('',*,*,#2708,.T.);
#3519=ORIENTED_EDGE('',*,*,#2724,.T.);
#3520=ORIENTED_EDGE('',*,*,#2721,.T.);
#3521=ORIENTED_EDGE('',*,*,#2705,.T.);
#3522=ORIENTED_EDGE('',*,*,#2733,.T.);
#3523=ORIENTED_EDGE('',*,*,#2730,.T.);
#3524=ORIENTED_EDGE('',*,*,#2710,.T.);
#3525=ORIENTED_EDGE('',*,*,#2729,.T.);
#3526=ORIENTED_EDGE('',*,*,#2726,.T.);
#3527=ORIENTED_EDGE('',*,*,#2740,.T.);
#3528=ORIENTED_EDGE('',*,*,#2737,.T.);
#3529=ORIENTED_EDGE('',*,*,#2734,.T.);
#4464=PLANE('',#5322);
#4465=PLANE('',#5350);
#4466=PLANE('',#5371);
#4467=PLANE('',#5372);
#4468=PLANE('',#5373);
#4469=PLANE('',#5374);
#4470=PLANE('',#5375);
#4471=PLANE('',#5376);
#4472=PLANE('',#5377);
#4473=PLANE('',#5378);
#4474=PLANE('',#5379);
#4475=PLANE('',#5380);
#4623=ADVANCED_FACE('',(#1247,#1121),#4464,.F.);
#4624=ADVANCED_FACE('',(#1248),#1013,.F.);
#4625=ADVANCED_FACE('',(#1249),#1014,.F.);
#4626=ADVANCED_FACE('',(#1250),#1015,.F.);
#4627=ADVANCED_FACE('',(#1251),#1016,.T.);
#4628=ADVANCED_FACE('',(#1252),#1017,.F.);
#4629=ADVANCED_FACE('',(#1253),#1018,.F.);
#4630=ADVANCED_FACE('',(#1254),#1019,.F.);
#4631=ADVANCED_FACE('',(#1255,#1122),#4465,.F.);
#4632=ADVANCED_FACE('',(#1256),#1020,.F.);
#4633=ADVANCED_FACE('',(#1257),#1021,.F.);
#4634=ADVANCED_FACE('',(#1258),#1022,.F.);
#4635=ADVANCED_FACE('',(#1259),#1023,.F.);
#4636=ADVANCED_FACE('',(#1260),#1024,.F.);
#4637=ADVANCED_FACE('',(#1261),#1025,.F.);
#4638=ADVANCED_FACE('',(#1262),#4466,.T.);
#4639=ADVANCED_FACE('',(#1263),#4467,.T.);
#4640=ADVANCED_FACE('',(#1264),#4468,.T.);
#4641=ADVANCED_FACE('',(#1265),#4469,.T.);
#4642=ADVANCED_FACE('',(#1266),#4470,.T.);
#4643=ADVANCED_FACE('',(#1267),#4471,.T.);
#4644=ADVANCED_FACE('',(#1268),#4472,.T.);
#4645=ADVANCED_FACE('',(#1269),#4473,.T.);
#4646=ADVANCED_FACE('',(#1270,#1123,#1124,#1125,#1126,#1127,#1128,#1129,
#1130),#4474,.T.);
#4647=ADVANCED_FACE('',(#1271,#1131,#1132,#1133,#1134),#4475,.F.);
#4888=CLOSED_SHELL('',(#4623,#4624,#4625,#4626,#4627,#4628,#4629,#4630,
#4631,#4632,#4633,#4634,#4635,#4636,#4637,#4638,#4639,#4640,#4641,#4642,
#4643,#4644,#4645,#4646,#4647));
#5321=AXIS2_PLACEMENT_3D('',#7710,#6094,#6095);
#5322=AXIS2_PLACEMENT_3D('',#7711,#6096,#6097);
#5323=AXIS2_PLACEMENT_3D('',#7714,#6098,#6099);
#5324=AXIS2_PLACEMENT_3D('',#7716,#6100,#6101);
#5325=AXIS2_PLACEMENT_3D('',#7718,#6102,#6103);
#5326=AXIS2_PLACEMENT_3D('',#7720,#6104,#6105);
#5327=AXIS2_PLACEMENT_3D('',#7722,#6106,#6107);
#5328=AXIS2_PLACEMENT_3D('',#7724,#6108,#6109);
#5329=AXIS2_PLACEMENT_3D('',#7726,#6110,#6111);
#5330=AXIS2_PLACEMENT_3D('',#7727,#6112,#6113);
#5331=AXIS2_PLACEMENT_3D('',#7729,#6114,#6115);
#5332=AXIS2_PLACEMENT_3D('',#7730,#6116,#6117);
#5333=AXIS2_PLACEMENT_3D('',#7735,#6120,#6121);
#5334=AXIS2_PLACEMENT_3D('',#7736,#6122,#6123);
#5335=AXIS2_PLACEMENT_3D('',#7741,#6126,#6127);
#5336=AXIS2_PLACEMENT_3D('',#7742,#6128,#6129);
#5337=AXIS2_PLACEMENT_3D('',#7746,#6131,#6132);
#5338=AXIS2_PLACEMENT_3D('',#7748,#6134,#6135);
#5339=AXIS2_PLACEMENT_3D('',#7750,#6136,#6137);
#5340=AXIS2_PLACEMENT_3D('',#7752,#6139,#6140);
#5341=AXIS2_PLACEMENT_3D('',#7756,#6142,#6143);
#5342=AXIS2_PLACEMENT_3D('',#7758,#6145,#6146);
#5343=AXIS2_PLACEMENT_3D('',#7760,#6147,#6148);
#5344=AXIS2_PLACEMENT_3D('',#7763,#6150,#6151);
#5345=AXIS2_PLACEMENT_3D('',#7764,#6152,#6153);
#5346=AXIS2_PLACEMENT_3D('',#7765,#6154,#6155);
#5347=AXIS2_PLACEMENT_3D('',#7767,#6156,#6157);
#5348=AXIS2_PLACEMENT_3D('',#7770,#6159,#6160);
#5349=AXIS2_PLACEMENT_3D('',#7771,#6161,#6162);
#5350=AXIS2_PLACEMENT_3D('',#7772,#6163,#6164);
#5351=AXIS2_PLACEMENT_3D('',#7774,#6165,#6166);
#5352=AXIS2_PLACEMENT_3D('',#7775,#6167,#6168);
#5353=AXIS2_PLACEMENT_3D('',#7777,#6169,#6170);
#5354=AXIS2_PLACEMENT_3D('',#7780,#6172,#6173);
#5355=AXIS2_PLACEMENT_3D('',#7781,#6174,#6175);
#5356=AXIS2_PLACEMENT_3D('',#7782,#6176,#6177);
#5357=AXIS2_PLACEMENT_3D('',#7784,#6178,#6179);
#5358=AXIS2_PLACEMENT_3D('',#7787,#6181,#6182);
#5359=AXIS2_PLACEMENT_3D('',#7788,#6183,#6184);
#5360=AXIS2_PLACEMENT_3D('',#7789,#6185,#6186);
#5361=AXIS2_PLACEMENT_3D('',#7791,#6187,#6188);
#5362=AXIS2_PLACEMENT_3D('',#7794,#6190,#6191);
#5363=AXIS2_PLACEMENT_3D('',#7795,#6192,#6193);
#5364=AXIS2_PLACEMENT_3D('',#7797,#6194,#6195);
#5365=AXIS2_PLACEMENT_3D('',#7800,#6197,#6198);
#5366=AXIS2_PLACEMENT_3D('',#7801,#6199,#6200);
#5367=AXIS2_PLACEMENT_3D('',#7803,#6201,#6202);
#5368=AXIS2_PLACEMENT_3D('',#7806,#6204,#6205);
#5369=AXIS2_PLACEMENT_3D('',#7807,#6206,#6207);
#5370=AXIS2_PLACEMENT_3D('',#7810,#6209,#6210);
#5371=AXIS2_PLACEMENT_3D('',#7811,#6211,#6212);
#5372=AXIS2_PLACEMENT_3D('',#7820,#6217,#6218);
#5373=AXIS2_PLACEMENT_3D('',#7826,#6222,#6223);
#5374=AXIS2_PLACEMENT_3D('',#7832,#6227,#6228);
#5375=AXIS2_PLACEMENT_3D('',#7838,#6232,#6233);
#5376=AXIS2_PLACEMENT_3D('',#7844,#6237,#6238);
#5377=AXIS2_PLACEMENT_3D('',#7850,#6242,#6243);
#5378=AXIS2_PLACEMENT_3D('',#7856,#6247,#6248);
#5379=AXIS2_PLACEMENT_3D('',#7859,#6251,#6252);
#5380=AXIS2_PLACEMENT_3D('',#7860,#6253,#6254);
#6094=DIRECTION('axis',(0.,0.,1.));
#6095=DIRECTION('refdir',(1.,0.,0.));
#6096=DIRECTION('center_axis',(0.,1.,0.));
#6097=DIRECTION('ref_axis',(1.,0.,0.));
#6098=DIRECTION('center_axis',(0.,-1.,0.));
#6099=DIRECTION('ref_axis',(1.,0.,0.));
#6100=DIRECTION('center_axis',(0.,1.,0.));
#6101=DIRECTION('ref_axis',(1.,0.,0.));
#6102=DIRECTION('center_axis',(0.,-1.,0.));
#6103=DIRECTION('ref_axis',(1.,0.,0.));
#6104=DIRECTION('center_axis',(0.,1.,0.));
#6105=DIRECTION('ref_axis',(1.,0.,0.));
#6106=DIRECTION('center_axis',(0.,-1.,0.));
#6107=DIRECTION('ref_axis',(1.,0.,0.));
#6108=DIRECTION('center_axis',(0.,1.,0.));
#6109=DIRECTION('ref_axis',(1.,0.,0.));
#6110=DIRECTION('center_axis',(0.,-1.,0.));
#6111=DIRECTION('ref_axis',(1.,0.,0.));
#6112=DIRECTION('center_axis',(0.,1.,0.));
#6113=DIRECTION('ref_axis',(1.,0.,0.));
#6114=DIRECTION('center_axis',(0.,-1.,0.));
#6115=DIRECTION('ref_axis',(1.,0.,0.));
#6116=DIRECTION('center_axis',(0.,1.,0.));
#6117=DIRECTION('ref_axis',(1.,0.,0.));
#6118=DIRECTION('',(0.,-1.,0.));
#6119=DIRECTION('',(0.,1.,0.));
#6120=DIRECTION('center_axis',(0.,1.,0.));
#6121=DIRECTION('ref_axis',(1.,0.,0.));
#6122=DIRECTION('center_axis',(0.,1.,0.));
#6123=DIRECTION('ref_axis',(-1.,0.,-1.22464679914735E-16));
#6124=DIRECTION('',(0.,-1.,0.));
#6125=DIRECTION('',(0.,1.,0.));
#6126=DIRECTION('center_axis',(0.,1.,0.));
#6127=DIRECTION('ref_axis',(1.,0.,0.));
#6128=DIRECTION('center_axis',(0.,1.,0.));
#6129=DIRECTION('ref_axis',(1.,0.,0.));
#6130=DIRECTION('',(0.,1.,0.));
#6131=DIRECTION('center_axis',(0.,1.,0.));
#6132=DIRECTION('ref_axis',(1.,0.,0.));
#6133=DIRECTION('',(0.,-1.,0.));
#6134=DIRECTION('center_axis',(0.,1.,0.));
#6135=DIRECTION('ref_axis',(1.,0.,0.));
#6136=DIRECTION('center_axis',(0.,-1.,0.));
#6137=DIRECTION('ref_axis',(1.,0.,0.));
#6138=DIRECTION('',(0.,1.,0.));
#6139=DIRECTION('center_axis',(0.,1.,0.));
#6140=DIRECTION('ref_axis',(1.,0.,0.));
#6141=DIRECTION('',(0.,1.,0.));
#6142=DIRECTION('center_axis',(0.,1.,0.));
#6143=DIRECTION('ref_axis',(1.,0.,0.));
#6144=DIRECTION('',(0.,-1.,0.));
#6145=DIRECTION('center_axis',(0.,1.,0.));
#6146=DIRECTION('ref_axis',(1.,0.,0.));
#6147=DIRECTION('center_axis',(0.,1.,0.));
#6148=DIRECTION('ref_axis',(1.,0.,0.));
#6149=DIRECTION('',(0.,1.,0.));
#6150=DIRECTION('center_axis',(0.,-1.,0.));
#6151=DIRECTION('ref_axis',(1.,0.,0.));
#6152=DIRECTION('center_axis',(0.,1.,0.));
#6153=DIRECTION('ref_axis',(1.,0.,0.));
#6154=DIRECTION('center_axis',(0.,1.,0.));
#6155=DIRECTION('ref_axis',(1.,0.,0.));
#6156=DIRECTION('center_axis',(0.,1.,0.));
#6157=DIRECTION('ref_axis',(1.,0.,0.));
#6158=DIRECTION('',(0.,1.,0.));
#6159=DIRECTION('center_axis',(0.,-1.,0.));
#6160=DIRECTION('ref_axis',(1.,0.,0.));
#6161=DIRECTION('center_axis',(0.,1.,0.));
#6162=DIRECTION('ref_axis',(1.,0.,0.));
#6163=DIRECTION('center_axis',(0.,1.,0.));
#6164=DIRECTION('ref_axis',(1.,0.,0.));
#6165=DIRECTION('center_axis',(0.,1.,0.));
#6166=DIRECTION('ref_axis',(1.,0.,0.));
#6167=DIRECTION('center_axis',(0.,1.,0.));
#6168=DIRECTION('ref_axis',(1.,0.,0.));
#6169=DIRECTION('center_axis',(0.,1.,0.));
#6170=DIRECTION('ref_axis',(1.,0.,0.));
#6171=DIRECTION('',(0.,1.,0.));
#6172=DIRECTION('center_axis',(0.,-1.,0.));
#6173=DIRECTION('ref_axis',(1.,0.,0.));
#6174=DIRECTION('center_axis',(0.,1.,0.));
#6175=DIRECTION('ref_axis',(1.,0.,0.));
#6176=DIRECTION('center_axis',(0.,1.,0.));
#6177=DIRECTION('ref_axis',(1.,0.,0.));
#6178=DIRECTION('center_axis',(0.,1.,0.));
#6179=DIRECTION('ref_axis',(1.,0.,0.));
#6180=DIRECTION('',(0.,1.,0.));
#6181=DIRECTION('center_axis',(0.,-1.,0.));
#6182=DIRECTION('ref_axis',(1.,0.,0.));
#6183=DIRECTION('center_axis',(0.,1.,0.));
#6184=DIRECTION('ref_axis',(1.,0.,0.));
#6185=DIRECTION('center_axis',(0.,1.,0.));
#6186=DIRECTION('ref_axis',(1.,0.,0.));
#6187=DIRECTION('center_axis',(0.,1.,0.));
#6188=DIRECTION('ref_axis',(1.,0.,0.));
#6189=DIRECTION('',(0.,1.,0.));
#6190=DIRECTION('center_axis',(0.,-1.,0.));
#6191=DIRECTION('ref_axis',(1.,0.,0.));
#6192=DIRECTION('center_axis',(0.,1.,0.));
#6193=DIRECTION('ref_axis',(1.,0.,0.));
#6194=DIRECTION('center_axis',(0.,1.,0.));
#6195=DIRECTION('ref_axis',(1.,0.,0.));
#6196=DIRECTION('',(0.,1.,0.));
#6197=DIRECTION('center_axis',(0.,-1.,0.));
#6198=DIRECTION('ref_axis',(1.,0.,0.));
#6199=DIRECTION('center_axis',(0.,1.,0.));
#6200=DIRECTION('ref_axis',(1.,0.,0.));
#6201=DIRECTION('center_axis',(0.,1.,0.));
#6202=DIRECTION('ref_axis',(1.,0.,0.));
#6203=DIRECTION('',(0.,1.,0.));
#6204=DIRECTION('center_axis',(0.,-1.,0.));
#6205=DIRECTION('ref_axis',(1.,0.,0.));
#6206=DIRECTION('center_axis',(0.,1.,0.));
#6207=DIRECTION('ref_axis',(1.,0.,0.));
#6208=DIRECTION('',(0.,1.,0.));
#6209=DIRECTION('center_axis',(0.,-1.,0.));
#6210=DIRECTION('ref_axis',(1.,0.,0.));
#6211=DIRECTION('center_axis',(-0.832050294337844,0.,-0.554700196225229));
#6212=DIRECTION('ref_axis',(-0.554700196225229,0.,0.832050294337844));
#6213=DIRECTION('',(0.554700196225229,0.,-0.832050294337844));
#6214=DIRECTION('',(0.,1.,0.));
#6215=DIRECTION('',(-0.554700196225229,0.,0.832050294337844));
#6216=DIRECTION('',(0.,1.,0.));
#6217=DIRECTION('center_axis',(0.,0.,-1.));
#6218=DIRECTION('ref_axis',(-1.,0.,0.));
#6219=DIRECTION('',(1.,0.,0.));
#6220=DIRECTION('',(-1.,0.,0.));
#6221=DIRECTION('',(0.,1.,0.));
#6222=DIRECTION('center_axis',(0.832050294337844,0.,-0.554700196225229));
#6223=DIRECTION('ref_axis',(-0.554700196225229,0.,-0.832050294337844));
#6224=DIRECTION('',(0.554700196225229,0.,0.832050294337844));
#6225=DIRECTION('',(-0.554700196225229,0.,-0.832050294337844));
#6226=DIRECTION('',(0.,1.,0.));
#6227=DIRECTION('center_axis',(1.,0.,0.));
#6228=DIRECTION('ref_axis',(0.,0.,-1.));
#6229=DIRECTION('',(0.,0.,1.));
#6230=DIRECTION('',(0.,0.,-1.));
#6231=DIRECTION('',(0.,1.,0.));
#6232=DIRECTION('center_axis',(0.894427190999916,0.,0.447213595499958));
#6233=DIRECTION('ref_axis',(0.447213595499958,0.,-0.894427190999916));
#6234=DIRECTION('',(-0.447213595499958,0.,0.894427190999916));
#6235=DIRECTION('',(0.447213595499958,0.,-0.894427190999916));
#6236=DIRECTION('',(0.,1.,0.));
#6237=DIRECTION('center_axis',(0.,0.,1.));
#6238=DIRECTION('ref_axis',(1.,0.,0.));
#6239=DIRECTION('',(-1.,0.,0.));
#6240=DIRECTION('',(1.,0.,0.));
#6241=DIRECTION('',(0.,1.,0.));
#6242=DIRECTION('center_axis',(-0.894427190999916,0.,0.447213595499958));
#6243=DIRECTION('ref_axis',(0.447213595499958,0.,0.894427190999916));
#6244=DIRECTION('',(-0.447213595499958,0.,-0.894427190999916));
#6245=DIRECTION('',(0.447213595499958,0.,0.894427190999916));
#6246=DIRECTION('',(0.,1.,0.));
#6247=DIRECTION('center_axis',(-1.,0.,0.));
#6248=DIRECTION('ref_axis',(0.,0.,1.));
#6249=DIRECTION('',(0.,0.,-1.));
#6250=DIRECTION('',(0.,0.,1.));
#6251=DIRECTION('center_axis',(0.,1.,0.));
#6252=DIRECTION('ref_axis',(0.,0.,1.));
#6253=DIRECTION('center_axis',(0.,1.,0.));
#6254=DIRECTION('ref_axis',(1.,0.,0.));
#7710=CARTESIAN_POINT('',(0.,0.,0.));
#7711=CARTESIAN_POINT('Origin',(0.,2.8,12.));
#7712=CARTESIAN_POINT('',(-2.60150387000671,2.8,10.0520067725117));
#7713=CARTESIAN_POINT('',(-2.99903459153175,2.8,10.7476855351806));
#7714=CARTESIAN_POINT('Origin',(-3.5,2.8,10.));
#7715=CARTESIAN_POINT('',(2.60150387000671,2.8,10.0520067725117));
#7716=CARTESIAN_POINT('Origin',(0.,2.8,12.));
#7717=CARTESIAN_POINT('',(2.99903459153175,2.8,10.7476855351806));
#7718=CARTESIAN_POINT('Origin',(3.5,2.8,10.));
#7719=CARTESIAN_POINT('',(2.99903459153175,2.8,13.2523144648194));
#7720=CARTESIAN_POINT('Origin',(0.,2.8,12.));
#7721=CARTESIAN_POINT('',(2.60150387000671,2.8,13.9479932274883));
#7722=CARTESIAN_POINT('Origin',(3.5,2.8,14.));
#7723=CARTESIAN_POINT('',(-2.60150387000671,2.8,13.9479932274883));
#7724=CARTESIAN_POINT('Origin',(0.,2.8,12.));
#7725=CARTESIAN_POINT('',(-2.99903459153175,2.8,13.2523144648194));
#7726=CARTESIAN_POINT('Origin',(-3.5,2.8,14.));
#7727=CARTESIAN_POINT('Origin',(0.,2.8,12.));
#7728=CARTESIAN_POINT('',(-1.2,2.8,12.));
#7729=CARTESIAN_POINT('Origin',(0.,2.8,12.));
#7730=CARTESIAN_POINT('Origin',(0.,2.5,12.));
#7731=CARTESIAN_POINT('',(-2.60150387000671,2.5,13.9479932274883));
#7732=CARTESIAN_POINT('',(-2.60150387000671,2.5,13.9479932274883));
#7733=CARTESIAN_POINT('',(2.60150387000671,2.5,13.9479932274883));
#7734=CARTESIAN_POINT('',(2.60150387000671,2.5,13.9479932274883));
#7735=CARTESIAN_POINT('Origin',(0.,2.5,12.));
#7736=CARTESIAN_POINT('Origin',(0.,2.5,12.));
#7737=CARTESIAN_POINT('',(-2.99903459153175,2.5,10.7476855351806));
#7738=CARTESIAN_POINT('',(-2.99903459153175,2.5,10.7476855351806));
#7739=CARTESIAN_POINT('',(-2.99903459153175,2.5,13.2523144648194));
#7740=CARTESIAN_POINT('',(-2.99903459153175,2.5,13.2523144648194));
#7741=CARTESIAN_POINT('Origin',(0.,2.5,12.));
#7742=CARTESIAN_POINT('Origin',(0.,2.5,12.));
#7743=CARTESIAN_POINT('',(2.99903459153175,2.5,10.7476855351806));
#7744=CARTESIAN_POINT('',(2.99903459153175,2.5,10.7476855351806));
#7745=CARTESIAN_POINT('',(2.99903459153175,2.5,13.2523144648194));
#7746=CARTESIAN_POINT('Origin',(0.,2.5,12.));
#7747=CARTESIAN_POINT('',(2.99903459153175,2.5,13.2523144648194));
#7748=CARTESIAN_POINT('Origin',(0.,2.5,12.));
#7749=CARTESIAN_POINT('',(-1.2,2.5,12.));
#7750=CARTESIAN_POINT('Origin',(0.,2.5,12.));
#7751=CARTESIAN_POINT('',(-1.2,2.5,12.));
#7752=CARTESIAN_POINT('Origin',(0.,2.5,12.));
#7753=CARTESIAN_POINT('',(-2.60150387000671,2.5,10.0520067725117));
#7754=CARTESIAN_POINT('',(-2.60150387000671,2.5,10.0520067725117));
#7755=CARTESIAN_POINT('',(2.60150387000671,2.5,10.0520067725117));
#7756=CARTESIAN_POINT('Origin',(0.,2.5,12.));
#7757=CARTESIAN_POINT('',(2.60150387000671,2.5,10.0520067725117));
#7758=CARTESIAN_POINT('Origin',(-3.5,2.4,10.));
#7759=CARTESIAN_POINT('',(-4.4,2.5,10.));
#7760=CARTESIAN_POINT('Origin',(-3.5,2.5,10.));
#7761=CARTESIAN_POINT('',(-4.4,3.1,10.));
#7762=CARTESIAN_POINT('',(-4.4,2.4,10.));
#7763=CARTESIAN_POINT('Origin',(-3.5,3.1,10.));
#7764=CARTESIAN_POINT('Origin',(-3.5,2.5,10.));
#7765=CARTESIAN_POINT('Origin',(-3.5,2.4,14.));
#7766=CARTESIAN_POINT('',(-4.4,2.5,14.));
#7767=CARTESIAN_POINT('Origin',(-3.5,2.5,14.));
#7768=CARTESIAN_POINT('',(-4.4,3.1,14.));
#7769=CARTESIAN_POINT('',(-4.4,2.4,14.));
#7770=CARTESIAN_POINT('Origin',(-3.5,3.1,14.));
#7771=CARTESIAN_POINT('Origin',(-3.5,2.5,14.));
#7772=CARTESIAN_POINT('Origin',(0.,2.5,13.25));
#7773=CARTESIAN_POINT('',(-1.,2.5,12.));
#7774=CARTESIAN_POINT('Origin',(0.,2.5,12.));
#7775=CARTESIAN_POINT('Origin',(3.5,2.4,10.));
#7776=CARTESIAN_POINT('',(2.6,2.5,10.));
#7777=CARTESIAN_POINT('Origin',(3.5,2.5,10.));
#7778=CARTESIAN_POINT('',(2.6,3.1,10.));
#7779=CARTESIAN_POINT('',(2.6,2.4,10.));
#7780=CARTESIAN_POINT('Origin',(3.5,3.1,10.));
#7781=CARTESIAN_POINT('Origin',(3.5,2.5,10.));
#7782=CARTESIAN_POINT('Origin',(3.5,2.4,14.));
#7783=CARTESIAN_POINT('',(2.6,2.5,14.));
#7784=CARTESIAN_POINT('Origin',(3.5,2.5,14.));
#7785=CARTESIAN_POINT('',(2.6,3.1,14.));
#7786=CARTESIAN_POINT('',(2.6,2.4,14.));
#7787=CARTESIAN_POINT('Origin',(3.5,3.1,14.));
#7788=CARTESIAN_POINT('Origin',(3.5,2.5,14.));
#7789=CARTESIAN_POINT('Origin',(-2.,2.4,5.));
#7790=CARTESIAN_POINT('',(-2.425,2.5,5.));
#7791=CARTESIAN_POINT('Origin',(-2.,2.5,5.));
#7792=CARTESIAN_POINT('',(-2.425,3.1,5.));
#7793=CARTESIAN_POINT('',(-2.425,2.4,5.));
#7794=CARTESIAN_POINT('Origin',(-2.,3.1,5.));
#7795=CARTESIAN_POINT('Origin',(2.,2.4,5.));
#7796=CARTESIAN_POINT('',(1.575,2.5,5.));
#7797=CARTESIAN_POINT('Origin',(2.,2.5,5.));
#7798=CARTESIAN_POINT('',(1.575,3.1,5.));
#7799=CARTESIAN_POINT('',(1.575,2.4,5.));
#7800=CARTESIAN_POINT('Origin',(2.,3.1,5.));
#7801=CARTESIAN_POINT('Origin',(0.,2.4,20.5));
#7802=CARTESIAN_POINT('',(-0.425,2.5,20.5));
#7803=CARTESIAN_POINT('Origin',(0.,2.5,20.5));
#7804=CARTESIAN_POINT('',(-0.425,3.1,20.5));
#7805=CARTESIAN_POINT('',(-0.425,2.4,20.5));
#7806=CARTESIAN_POINT('Origin',(0.,3.1,20.5));
#7807=CARTESIAN_POINT('Origin',(0.,2.4,12.));
#7808=CARTESIAN_POINT('',(-1.,3.1,12.));
#7809=CARTESIAN_POINT('',(-1.,2.4,12.));
#7810=CARTESIAN_POINT('Origin',(0.,3.1,12.));
#7811=CARTESIAN_POINT('Origin',(-3.,2.5,4.5));
#7812=CARTESIAN_POINT('',(-6.,2.5,9.));
#7813=CARTESIAN_POINT('',(-3.,2.5,4.5));
#7814=CARTESIAN_POINT('',(-6.,2.5,9.));
#7815=CARTESIAN_POINT('',(-6.,3.1,9.));
#7816=CARTESIAN_POINT('',(-6.,2.5,9.));
#7817=CARTESIAN_POINT('',(-3.,3.1,4.5));
#7818=CARTESIAN_POINT('',(-6.,3.1,9.));
#7819=CARTESIAN_POINT('',(-3.,2.5,4.5));
#7820=CARTESIAN_POINT('Origin',(3.,2.5,4.5));
#7821=CARTESIAN_POINT('',(3.,2.5,4.5));
#7822=CARTESIAN_POINT('',(-3.,2.5,4.5));
#7823=CARTESIAN_POINT('',(3.,3.1,4.5));
#7824=CARTESIAN_POINT('',(-3.,3.1,4.5));
#7825=CARTESIAN_POINT('',(3.,2.5,4.5));
#7826=CARTESIAN_POINT('Origin',(6.,2.5,9.));
#7827=CARTESIAN_POINT('',(6.,2.5,9.));
#7828=CARTESIAN_POINT('',(3.,2.5,4.5));
#7829=CARTESIAN_POINT('',(6.,3.1,9.));
#7830=CARTESIAN_POINT('',(3.,3.1,4.5));
#7831=CARTESIAN_POINT('',(6.,2.5,9.));
#7832=CARTESIAN_POINT('Origin',(6.,2.5,15.));
#7833=CARTESIAN_POINT('',(6.,2.5,15.));
#7834=CARTESIAN_POINT('',(6.,2.5,9.));
#7835=CARTESIAN_POINT('',(6.,3.1,15.));
#7836=CARTESIAN_POINT('',(6.,3.1,9.));
#7837=CARTESIAN_POINT('',(6.,2.5,15.));
#7838=CARTESIAN_POINT('Origin',(2.5,2.5,22.));
#7839=CARTESIAN_POINT('',(2.5,2.5,22.));
#7840=CARTESIAN_POINT('',(6.,2.5,15.));
#7841=CARTESIAN_POINT('',(2.5,3.1,22.));
#7842=CARTESIAN_POINT('',(6.,3.1,15.));
#7843=CARTESIAN_POINT('',(2.5,2.5,22.));
#7844=CARTESIAN_POINT('Origin',(-2.5,2.5,22.));
#7845=CARTESIAN_POINT('',(-2.5,2.5,22.));
#7846=CARTESIAN_POINT('',(2.5,2.5,22.));
#7847=CARTESIAN_POINT('',(-2.5,3.1,22.));
#7848=CARTESIAN_POINT('',(2.5,3.1,22.));
#7849=CARTESIAN_POINT('',(-2.5,2.5,22.));
#7850=CARTESIAN_POINT('Origin',(-6.,2.5,15.));
#7851=CARTESIAN_POINT('',(-6.,2.5,15.));
#7852=CARTESIAN_POINT('',(-2.5,2.5,22.));
#7853=CARTESIAN_POINT('',(-6.,3.1,15.));
#7854=CARTESIAN_POINT('',(-2.5,3.1,22.));
#7855=CARTESIAN_POINT('',(-6.,2.5,15.));
#7856=CARTESIAN_POINT('Origin',(-6.,2.5,9.));
#7857=CARTESIAN_POINT('',(-6.,2.5,15.));
#7858=CARTESIAN_POINT('',(-6.,3.1,15.));
#7859=CARTESIAN_POINT('Origin',(0.,3.1,13.25));
#7860=CARTESIAN_POINT('Origin',(0.,2.5,13.25));
#9321=UNCERTAINTY_MEASURE_WITH_UNIT(LENGTH_MEASURE(0.001),#9392,
'DISTANCE_ACCURACY_VALUE',
'Maximum model space distance between geometric entities at asserted c
onnectivities');
#9354=UNCERTAINTY_MEASURE_WITH_UNIT(LENGTH_MEASURE(0.001),#9392,
'DISTANCE_ACCURACY_VALUE',
'Maximum model space distance between geometric entities at asserted c
onnectivities');
#9358=(
GEOMETRIC_REPRESENTATION_CONTEXT(3)
GLOBAL_UNCERTAINTY_ASSIGNED_CONTEXT((#9321))
GLOBAL_UNIT_ASSIGNED_CONTEXT((#9392,#9394,#9395))
REPRESENTATION_CONTEXT('','3D')
);
#9391=(
GEOMETRIC_REPRESENTATION_CONTEXT(3)
GLOBAL_UNCERTAINTY_ASSIGNED_CONTEXT((#9354))
GLOBAL_UNIT_ASSIGNED_CONTEXT((#9392,#9394,#9395))
REPRESENTATION_CONTEXT('','3D')
);
#9392=(
LENGTH_UNIT()
NAMED_UNIT(*)
SI_UNIT(.CENTI.,.METRE.)
);
#9394=(
NAMED_UNIT(*)
PLANE_ANGLE_UNIT()
SI_UNIT($,.RADIAN.)
);
#9395=(
NAMED_UNIT(*)
SI_UNIT($,.STERADIAN.)
SOLID_ANGLE_UNIT()
);
#9399=SHAPE_DEFINITION_REPRESENTATION(#9435,#9523);
#9435=PRODUCT_DEFINITION_SHAPE('',$,#9560);
#9523=SHAPE_REPRESENTATION('',(#5321),#9358);
#9556=PRODUCT_DEFINITION_CONTEXT('part definition',#9666,'design');
#9560=PRODUCT_DEFINITION('Side plate (1)','Side plate (1)',#9596,#9556);
#9596=PRODUCT_DEFINITION_FORMATION('',$,#9671);
#9666=APPLICATION_CONTEXT(
'Core Data for Automotive Mechanical Design Process');
#9667=PRODUCT_CONTEXT('part definition',#9666,'mechanical');
#9671=PRODUCT('Side plate (1)','Side plate (1)','Side plate (1)',(#9667));
#9746=COLOUR_RGB('Sky Blue',0.24,0.69,0.87);
#9747=FILL_AREA_STYLE_COLOUR('',#9746);
#9748=FILL_AREA_STYLE('',(#9747));
#9749=SURFACE_STYLE_FILL_AREA(#9748);
#9750=SURFACE_SIDE_STYLE('',(#9749));
#9751=SURFACE_STYLE_USAGE(.BOTH.,#9750);
#9752=PRESENTATION_STYLE_ASSIGNMENT((#9751));
ENDSEC;
END-ISO-10303-21;
